ISO-10303-21;
HEADER;
/* Generated by software containing ST-Developer
 * from STEP Tools, Inc. (www.steptools.com) 
 */

FILE_DESCRIPTION(
/* description */ ('Shaft runout checking stand'),
/* implementation_level */ '2;1');

FILE_NAME(
/* name */ 'Flat Washer - M5.step',
/* time_stamp */ '2026-11-02T21:12:33-08:00',
/* author */ (''),
/* organization */ (''),
/* preprocessor_version */ 'ST-DEVELOPER v20.2',
/* originating_system */ 'Autodesk Translation Framework v15.17.0.0',
/* authorisation */ '');

FILE_SCHEMA (('AUTOMOTIVE_DESIGN { 1 0 10303 214 3 1 1 }'));
ENDSEC;

DATA;
#10=MECHANICAL_DESIGN_GEOMETRIC_PRESENTATION_REPRESENTATION('',(#466),#11748);
#359=CONICAL_SURFACE('',#6851,0.275,0.785398163397449);
#380=SHAPE_REPRESENTATION_RELATIONSHIP('SRR','None',#11929,#423);
#423=ADVANCED_BREP_SHAPE_REPRESENTATION('',(#517),#11705);
#466=STYLED_ITEM('',(#12170),#517);
#517=MANIFOLD_SOLID_BREP('Body1',#6209);
#589=FACE_BOUND('',#1515,.T.);
#590=FACE_BOUND('',#1518,.T.);
#703=CIRCLE('',#6852,0.285);
#704=CIRCLE('',#6853,0.265);
#705=CIRCLE('',#6855,0.265);
#706=CIRCLE('',#6857,0.5);
#707=CIRCLE('',#6859,0.5);
#952=CYLINDRICAL_SURFACE('',#6854,0.265);
#953=CYLINDRICAL_SURFACE('',#6858,0.5);
#1117=FACE_OUTER_BOUND('',#1512,.T.);
#1118=FACE_OUTER_BOUND('',#1513,.T.);
#1119=FACE_OUTER_BOUND('',#1514,.T.);
#1120=FACE_OUTER_BOUND('',#1516,.T.);
#1121=FACE_OUTER_BOUND('',#1517,.T.);
#1512=EDGE_LOOP('',(#4532,#4533,#4534,#4535));
#1513=EDGE_LOOP('',(#4536,#4537,#4538,#4539));
#1514=EDGE_LOOP('',(#4540));
#1515=EDGE_LOOP('',(#4541));
#1516=EDGE_LOOP('',(#4542,#4543,#4544,#4545));
#1517=EDGE_LOOP('',(#4546));
#1518=EDGE_LOOP('',(#4547));
#2075=LINE('',#9934,#2542);
#2076=LINE('',#9938,#2543);
#2077=LINE('',#9945,#2544);
#2542=VECTOR('',#7920,0.275);
#2543=VECTOR('',#7925,0.265);
#2544=VECTOR('',#7934,0.5);
#2967=VERTEX_POINT('',#9931);
#2968=VERTEX_POINT('',#9933);
#2969=VERTEX_POINT('',#9937);
#2970=VERTEX_POINT('',#9941);
#2971=VERTEX_POINT('',#9944);
#3552=EDGE_CURVE('',#2967,#2967,#703,.T.);
#3553=EDGE_CURVE('',#2967,#2968,#2075,.T.);
#3554=EDGE_CURVE('',#2968,#2968,#704,.T.);
#3555=EDGE_CURVE('',#2968,#2969,#2076,.T.);
#3556=EDGE_CURVE('',#2969,#2969,#705,.T.);
#3557=EDGE_CURVE('',#2970,#2970,#706,.T.);
#3558=EDGE_CURVE('',#2970,#2971,#2077,.T.);
#3559=EDGE_CURVE('',#2971,#2971,#707,.T.);
#4532=ORIENTED_EDGE('',*,*,#3552,.T.);
#4533=ORIENTED_EDGE('',*,*,#3553,.T.);
#4534=ORIENTED_EDGE('',*,*,#3554,.T.);
#4535=ORIENTED_EDGE('',*,*,#3553,.F.);
#4536=ORIENTED_EDGE('',*,*,#3554,.F.);
#4537=ORIENTED_EDGE('',*,*,#3555,.T.);
#4538=ORIENTED_EDGE('',*,*,#3556,.T.);
#4539=ORIENTED_EDGE('',*,*,#3555,.F.);
#4540=ORIENTED_EDGE('',*,*,#3557,.T.);
#4541=ORIENTED_EDGE('',*,*,#3552,.F.);
#4542=ORIENTED_EDGE('',*,*,#3557,.F.);
#4543=ORIENTED_EDGE('',*,*,#3558,.T.);
#4544=ORIENTED_EDGE('',*,*,#3559,.T.);
#4545=ORIENTED_EDGE('',*,*,#3558,.F.);
#4546=ORIENTED_EDGE('',*,*,#3559,.F.);
#4547=ORIENTED_EDGE('',*,*,#3556,.F.);
#5669=PLANE('',#6856);
#5670=PLANE('',#6860);
#5917=ADVANCED_FACE('',(#1117),#359,.F.);
#5918=ADVANCED_FACE('',(#1118),#952,.F.);
#5919=ADVANCED_FACE('',(#1119,#589),#5669,.T.);
#5920=ADVANCED_FACE('',(#1120),#953,.T.);
#5921=ADVANCED_FACE('',(#1121,#590),#5670,.F.);
#6209=CLOSED_SHELL('',(#5917,#5918,#5919,#5920,#5921));
#6850=AXIS2_PLACEMENT_3D('',#9929,#7914,#7915);
#6851=AXIS2_PLACEMENT_3D('',#9930,#7916,#7917);
#6852=AXIS2_PLACEMENT_3D('',#9932,#7918,#7919);
#6853=AXIS2_PLACEMENT_3D('',#9935,#7921,#7922);
#6854=AXIS2_PLACEMENT_3D('',#9936,#7923,#7924);
#6855=AXIS2_PLACEMENT_3D('',#9939,#7926,#7927);
#6856=AXIS2_PLACEMENT_3D('',#9940,#7928,#7929);
#6857=AXIS2_PLACEMENT_3D('',#9942,#7930,#7931);
#6858=AXIS2_PLACEMENT_3D('',#9943,#7932,#7933);
#6859=AXIS2_PLACEMENT_3D('',#9946,#7935,#7936);
#6860=AXIS2_PLACEMENT_3D('',#9947,#7937,#7938);
#7914=DIRECTION('axis',(0.,0.,1.));
#7915=DIRECTION('refdir',(1.,0.,0.));
#7916=DIRECTION('center_axis',(0.,1.,0.));
#7917=DIRECTION('ref_axis',(1.,0.,0.));
#7918=DIRECTION('center_axis',(0.,1.,0.));
#7919=DIRECTION('ref_axis',(1.,0.,0.));
#7920=DIRECTION('',(0.707106781186548,-0.707106781186547,-8.65956056235494E-17));
#7921=DIRECTION('center_axis',(0.,-1.,0.));
#7922=DIRECTION('ref_axis',(1.,0.,0.));
#7923=DIRECTION('center_axis',(0.,1.,0.));
#7924=DIRECTION('ref_axis',(1.,0.,0.));
#7925=DIRECTION('',(0.,-1.,0.));
#7926=DIRECTION('center_axis',(0.,-1.,0.));
#7927=DIRECTION('ref_axis',(1.,0.,0.));
#7928=DIRECTION('center_axis',(0.,1.,0.));
#7929=DIRECTION('ref_axis',(1.,0.,0.));
#7930=DIRECTION('center_axis',(0.,1.,0.));
#7931=DIRECTION('ref_axis',(1.,0.,0.));
#7932=DIRECTION('center_axis',(0.,1.,0.));
#7933=DIRECTION('ref_axis',(1.,0.,0.));
#7934=DIRECTION('',(0.,-1.,0.));
#7935=DIRECTION('center_axis',(0.,1.,0.));
#7936=DIRECTION('ref_axis',(1.,0.,0.));
#7937=DIRECTION('center_axis',(0.,1.,0.));
#7938=DIRECTION('ref_axis',(1.,0.,0.));
#9929=CARTESIAN_POINT('',(0.,0.,0.));
#9930=CARTESIAN_POINT('Origin',(0.,0.09,0.));
#9931=CARTESIAN_POINT('',(-0.285,0.1,3.49024337756996E-17));
#9932=CARTESIAN_POINT('Origin',(0.,0.1,0.));
#9933=CARTESIAN_POINT('',(-0.265,0.08,-3.24531401774049E-17));
#9934=CARTESIAN_POINT('',(-0.275,0.09,3.36777869765522E-17));
#9935=CARTESIAN_POINT('Origin',(0.,0.08,0.));
#9936=CARTESIAN_POINT('Origin',(0.,0.,0.));
#9937=CARTESIAN_POINT('',(-0.265,0.,3.24531401774049E-17));
#9938=CARTESIAN_POINT('',(-0.265,0.,3.24531401774049E-17));
#9939=CARTESIAN_POINT('Origin',(0.,0.,0.));
#9940=CARTESIAN_POINT('Origin',(0.,0.1,0.));
#9941=CARTESIAN_POINT('',(-0.5,0.1,6.12323399573677E-17));
#9942=CARTESIAN_POINT('Origin',(0.,0.1,0.));
#9943=CARTESIAN_POINT('Origin',(0.,0.,0.));
#9944=CARTESIAN_POINT('',(-0.5,0.,6.12323399573677E-17));
#9945=CARTESIAN_POINT('',(-0.5,0.,6.12323399573677E-17));
#9946=CARTESIAN_POINT('Origin',(0.,0.,0.));
#9947=CARTESIAN_POINT('Origin',(0.,0.,0.));
#11656=UNCERTAINTY_MEASURE_WITH_UNIT(LENGTH_MEASURE(0.001),#11749,
'DISTANCE_ACCURACY_VALUE',
'Maximum model space distance between geometric entities at asserted c
onnectivities');
#11699=UNCERTAINTY_MEASURE_WITH_UNIT(LENGTH_MEASURE(0.001),#11749,
'DISTANCE_ACCURACY_VALUE',
'Maximum model space distance between geometric entities at asserted c
onnectivities');
#11705=(
GEOMETRIC_REPRESENTATION_CONTEXT(3)
GLOBAL_UNCERTAINTY_ASSIGNED_CONTEXT((#11656))
GLOBAL_UNIT_ASSIGNED_CONTEXT((#11749,#11751,#11752))
REPRESENTATION_CONTEXT('','3D')
);
#11748=(
GEOMETRIC_REPRESENTATION_CONTEXT(3)
GLOBAL_UNCERTAINTY_ASSIGNED_CONTEXT((#11699))
GLOBAL_UNIT_ASSIGNED_CONTEXT((#11749,#11751,#11752))
REPRESENTATION_CONTEXT('','3D')
);
#11749=(
LENGTH_UNIT()
NAMED_UNIT(*)
SI_UNIT(.CENTI.,.METRE.)
);
#11751=(
NAMED_UNIT(*)
PLANE_ANGLE_UNIT()
SI_UNIT($,.RADIAN.)
);
#11752=(
NAMED_UNIT(*)
SI_UNIT($,.STERADIAN.)
SOLID_ANGLE_UNIT()
);
#11758=SHAPE_DEFINITION_REPRESENTATION(#11806,#11929);
#11806=PRODUCT_DEFINITION_SHAPE('',$,#11978);
#11929=SHAPE_REPRESENTATION('',(#6850),#11705);
#11972=PRODUCT_DEFINITION_CONTEXT('part definition',#12118,'design');
#11978=PRODUCT_DEFINITION('Flat Washer - M5','Flat Washer - M5',#12026,
#11972);
#12026=PRODUCT_DEFINITION_FORMATION('',$,#12125);
#12118=APPLICATION_CONTEXT(
'Core Data for Automotive Mechanical Design Process');
#12119=PRODUCT_CONTEXT('part definition',#12118,'mechanical');
#12125=PRODUCT('Flat Washer - M5','Flat Washer - M5','Flat Washer - M5',
(#12119));
#12170=PRESENTATION_STYLE_ASSIGNMENT((#12175));
#12175=SURFACE_STYLE_USAGE(.BOTH.,#12180);
#12180=SURFACE_SIDE_STYLE('',(#12185));
#12185=SURFACE_STYLE_FILL_AREA(#12190);
#12190=FILL_AREA_STYLE('CAD Library Painted - Steel gray',(#12195));
#12195=FILL_AREA_STYLE_COLOUR('CAD Library Painted - Steel gray',#12200);
#12200=COLOUR_RGB('CAD Library Painted - Steel gray',0.592156862745098,
0.631372549019608,0.67843137254902);
ENDSEC;
END-ISO-10303-21;
